ISO-10303-21;
HEADER;
/* Generated by software containing ST-Developer
 * from STEP Tools, Inc. (www.steptools.com) 
 */

FILE_DESCRIPTION(
/* description */ ('Compact intermittent indexer'),
/* implementation_level */ '2;1');

FILE_NAME(
/* name */ 'M4x10 Cap Screw.step',
/* time_stamp */ '2026-10-29T16:32:17-07:00',
/* author */ (''),
/* organization */ (''),
/* preprocessor_version */ 'ST-DEVELOPER v20.2',
/* originating_system */ 'Autodesk Translation Framework v15.17.0.0',
/* authorisation */ '');

FILE_SCHEMA (('AUTOMOTIVE_DESIGN { 1 0 10303 214 3 1 1 }'));
ENDSEC;

DATA;
#10=MECHANICAL_DESIGN_GEOMETRIC_PRESENTATION_REPRESENTATION('',(#284),#10837);
#194=ORIENTED_CLOSED_SHELL('',*,#5657,.F.);
#203=CONICAL_SURFACE('',#6456,0.325,0.785398163397448);
#204=CONICAL_SURFACE('',#6460,0.335,0.785398163397448);
#205=CONICAL_SURFACE('',#6464,0.21,0.463647609000806);
#208=BREP_WITH_VOIDS('Body1',#5658,(#194));
#228=SHAPE_REPRESENTATION_RELATIONSHIP('SRR','None',#10964,#252);
#252=ADVANCED_BREP_SHAPE_REPRESENTATION('',(#208),#10831);
#284=STYLED_ITEM('',(#11173),#208);
#454=FACE_BOUND('',#1331,.T.);
#589=PLANE('',#6444);
#590=PLANE('',#6445);
#591=PLANE('',#6446);
#592=PLANE('',#6447);
#593=PLANE('',#6448);
#594=PLANE('',#6449);
#595=PLANE('',#6450);
#596=PLANE('',#6451);
#597=PLANE('',#6452);
#598=PLANE('',#6454);
#599=PLANE('',#6462);
#888=FACE_OUTER_BOUND('',#1317,.T.);
#889=FACE_OUTER_BOUND('',#1318,.T.);
#890=FACE_OUTER_BOUND('',#1319,.T.);
#891=FACE_OUTER_BOUND('',#1320,.T.);
#892=FACE_OUTER_BOUND('',#1321,.T.);
#893=FACE_OUTER_BOUND('',#1322,.T.);
#894=FACE_OUTER_BOUND('',#1323,.T.);
#895=FACE_OUTER_BOUND('',#1324,.T.);
#896=FACE_OUTER_BOUND('',#1325,.T.);
#897=FACE_OUTER_BOUND('',#1326,.T.);
#898=FACE_OUTER_BOUND('',#1327,.T.);
#899=FACE_OUTER_BOUND('',#1328,.T.);
#900=FACE_OUTER_BOUND('',#1329,.T.);
#901=FACE_OUTER_BOUND('',#1330,.T.);
#902=FACE_OUTER_BOUND('',#1332,.T.);
#903=FACE_OUTER_BOUND('',#1333,.T.);
#1317=EDGE_LOOP('',(#4672,#4673,#4674,#4675));
#1318=EDGE_LOOP('',(#4676,#4677,#4678,#4679));
#1319=EDGE_LOOP('',(#4680,#4681,#4682,#4683));
#1320=EDGE_LOOP('',(#4684,#4685,#4686,#4687));
#1321=EDGE_LOOP('',(#4688,#4689,#4690,#4691));
#1322=EDGE_LOOP('',(#4692,#4693,#4694,#4695));
#1323=EDGE_LOOP('',(#4696,#4697,#4698,#4699,#4700,#4701));
#1324=EDGE_LOOP('',(#4702,#4703,#4704,#4705,#4706,#4707));
#1325=EDGE_LOOP('',(#4708));
#1326=EDGE_LOOP('',(#4709));
#1327=EDGE_LOOP('',(#4710,#4711,#4712,#4713));
#1328=EDGE_LOOP('',(#4714,#4715,#4716,#4717));
#1329=EDGE_LOOP('',(#4718,#4719,#4720,#4721));
#1330=EDGE_LOOP('',(#4722));
#1331=EDGE_LOOP('',(#4723));
#1332=EDGE_LOOP('',(#4724,#4725,#4726,#4727));
#1333=EDGE_LOOP('',(#4728,#4729,#4730,#4731));
#1633=LINE('',#10105,#1991);
#1634=LINE('',#10107,#1992);
#1635=LINE('',#10109,#1993);
#1636=LINE('',#10110,#1994);
#1637=LINE('',#10113,#1995);
#1638=LINE('',#10115,#1996);
#1639=LINE('',#10116,#1997);
#1640=LINE('',#10119,#1998);
#1641=LINE('',#10121,#1999);
#1642=LINE('',#10122,#2000);
#1643=LINE('',#10125,#2001);
#1644=LINE('',#10127,#2002);
#1645=LINE('',#10128,#2003);
#1646=LINE('',#10131,#2004);
#1647=LINE('',#10133,#2005);
#1648=LINE('',#10134,#2006);
#1649=LINE('',#10136,#2007);
#1650=LINE('',#10137,#2008);
#1651=LINE('',#10149,#2009);
#1652=LINE('',#10153,#2010);
#1653=LINE('',#10157,#2011);
#1654=LINE('',#10164,#2012);
#1655=LINE('',#10166,#2013);
#1991=VECTOR('',#7901,1.);
#1992=VECTOR('',#7902,1.);
#1993=VECTOR('',#7903,1.);
#1994=VECTOR('',#7904,1.);
#1995=VECTOR('',#7907,1.);
#1996=VECTOR('',#7908,1.);
#1997=VECTOR('',#7909,1.);
#1998=VECTOR('',#7912,1.);
#1999=VECTOR('',#7913,1.);
#2000=VECTOR('',#7914,1.);
#2001=VECTOR('',#7917,1.);
#2002=VECTOR('',#7918,1.);
#2003=VECTOR('',#7919,1.);
#2004=VECTOR('',#7922,1.);
#2005=VECTOR('',#7923,1.);
#2006=VECTOR('',#7924,1.);
#2007=VECTOR('',#7927,1.);
#2008=VECTOR('',#7928,1.);
#2009=VECTOR('',#7945,0.325);
#2010=VECTOR('',#7950,0.35);
#2011=VECTOR('',#7955,0.335);
#2012=VECTOR('',#7964,0.21);
#2013=VECTOR('',#7967,0.2);
#2399=CIRCLE('',#6453,0.1954);
#2400=CIRCLE('',#6455,0.3);
#2401=CIRCLE('',#6457,0.35);
#2402=CIRCLE('',#6459,0.35);
#2403=CIRCLE('',#6461,0.32);
#2404=CIRCLE('',#6463,0.22);
#2405=CIRCLE('',#6465,0.1954);
#2811=VERTEX_POINT('',#10103);
#2812=VERTEX_POINT('',#10104);
#2813=VERTEX_POINT('',#10106);
#2814=VERTEX_POINT('',#10108);
#2815=VERTEX_POINT('',#10112);
#2816=VERTEX_POINT('',#10114);
#2817=VERTEX_POINT('',#10118);
#2818=VERTEX_POINT('',#10120);
#2819=VERTEX_POINT('',#10124);
#2820=VERTEX_POINT('',#10126);
#2821=VERTEX_POINT('',#10130);
#2822=VERTEX_POINT('',#10132);
#2823=VERTEX_POINT('',#10141);
#2824=VERTEX_POINT('',#10144);
#2825=VERTEX_POINT('',#10147);
#2826=VERTEX_POINT('',#10151);
#2827=VERTEX_POINT('',#10155);
#2828=VERTEX_POINT('',#10159);
#2829=VERTEX_POINT('',#10162);
#3458=EDGE_CURVE('',#2811,#2812,#1633,.T.);
#3459=EDGE_CURVE('',#2812,#2813,#1634,.T.);
#3460=EDGE_CURVE('',#2813,#2814,#1635,.T.);
#3461=EDGE_CURVE('',#2811,#2814,#1636,.T.);
#3462=EDGE_CURVE('',#2812,#2815,#1637,.T.);
#3463=EDGE_CURVE('',#2815,#2816,#1638,.T.);
#3464=EDGE_CURVE('',#2816,#2813,#1639,.T.);
#3465=EDGE_CURVE('',#2815,#2817,#1640,.T.);
#3466=EDGE_CURVE('',#2817,#2818,#1641,.T.);
#3467=EDGE_CURVE('',#2818,#2816,#1642,.T.);
#3468=EDGE_CURVE('',#2817,#2819,#1643,.T.);
#3469=EDGE_CURVE('',#2819,#2820,#1644,.T.);
#3470=EDGE_CURVE('',#2820,#2818,#1645,.T.);
#3471=EDGE_CURVE('',#2819,#2821,#1646,.T.);
#3472=EDGE_CURVE('',#2821,#2822,#1647,.T.);
#3473=EDGE_CURVE('',#2822,#2820,#1648,.T.);
#3474=EDGE_CURVE('',#2821,#2811,#1649,.T.);
#3475=EDGE_CURVE('',#2814,#2822,#1650,.T.);
#3476=EDGE_CURVE('',#2823,#2823,#2399,.T.);
#3477=EDGE_CURVE('',#2824,#2824,#2400,.T.);
#3478=EDGE_CURVE('',#2825,#2825,#2401,.T.);
#3479=EDGE_CURVE('',#2825,#2824,#1651,.T.);
#3480=EDGE_CURVE('',#2826,#2826,#2402,.T.);
#3481=EDGE_CURVE('',#2826,#2825,#1652,.T.);
#3482=EDGE_CURVE('',#2827,#2827,#2403,.T.);
#3483=EDGE_CURVE('',#2827,#2826,#1653,.T.);
#3484=EDGE_CURVE('',#2828,#2828,#2404,.T.);
#3485=EDGE_CURVE('',#2829,#2829,#2405,.F.);
#3486=EDGE_CURVE('',#2829,#2828,#1654,.T.);
#3487=EDGE_CURVE('',#2823,#2829,#1655,.T.);
#4672=ORIENTED_EDGE('',*,*,#3458,.T.);
#4673=ORIENTED_EDGE('',*,*,#3459,.T.);
#4674=ORIENTED_EDGE('',*,*,#3460,.T.);
#4675=ORIENTED_EDGE('',*,*,#3461,.F.);
#4676=ORIENTED_EDGE('',*,*,#3462,.T.);
#4677=ORIENTED_EDGE('',*,*,#3463,.T.);
#4678=ORIENTED_EDGE('',*,*,#3464,.T.);
#4679=ORIENTED_EDGE('',*,*,#3459,.F.);
#4680=ORIENTED_EDGE('',*,*,#3465,.T.);
#4681=ORIENTED_EDGE('',*,*,#3466,.T.);
#4682=ORIENTED_EDGE('',*,*,#3467,.T.);
#4683=ORIENTED_EDGE('',*,*,#3463,.F.);
#4684=ORIENTED_EDGE('',*,*,#3468,.T.);
#4685=ORIENTED_EDGE('',*,*,#3469,.T.);
#4686=ORIENTED_EDGE('',*,*,#3470,.T.);
#4687=ORIENTED_EDGE('',*,*,#3466,.F.);
#4688=ORIENTED_EDGE('',*,*,#3471,.T.);
#4689=ORIENTED_EDGE('',*,*,#3472,.T.);
#4690=ORIENTED_EDGE('',*,*,#3473,.T.);
#4691=ORIENTED_EDGE('',*,*,#3469,.F.);
#4692=ORIENTED_EDGE('',*,*,#3474,.T.);
#4693=ORIENTED_EDGE('',*,*,#3461,.T.);
#4694=ORIENTED_EDGE('',*,*,#3475,.T.);
#4695=ORIENTED_EDGE('',*,*,#3472,.F.);
#4696=ORIENTED_EDGE('',*,*,#3474,.F.);
#4697=ORIENTED_EDGE('',*,*,#3471,.F.);
#4698=ORIENTED_EDGE('',*,*,#3468,.F.);
#4699=ORIENTED_EDGE('',*,*,#3465,.F.);
#4700=ORIENTED_EDGE('',*,*,#3462,.F.);
#4701=ORIENTED_EDGE('',*,*,#3458,.F.);
#4702=ORIENTED_EDGE('',*,*,#3475,.F.);
#4703=ORIENTED_EDGE('',*,*,#3460,.F.);
#4704=ORIENTED_EDGE('',*,*,#3464,.F.);
#4705=ORIENTED_EDGE('',*,*,#3467,.F.);
#4706=ORIENTED_EDGE('',*,*,#3470,.F.);
#4707=ORIENTED_EDGE('',*,*,#3473,.F.);
#4708=ORIENTED_EDGE('',*,*,#3476,.F.);
#4709=ORIENTED_EDGE('',*,*,#3477,.F.);
#4710=ORIENTED_EDGE('',*,*,#3478,.F.);
#4711=ORIENTED_EDGE('',*,*,#3479,.T.);
#4712=ORIENTED_EDGE('',*,*,#3477,.T.);
#4713=ORIENTED_EDGE('',*,*,#3479,.F.);
#4714=ORIENTED_EDGE('',*,*,#3480,.F.);
#4715=ORIENTED_EDGE('',*,*,#3481,.T.);
#4716=ORIENTED_EDGE('',*,*,#3478,.T.);
#4717=ORIENTED_EDGE('',*,*,#3481,.F.);
#4718=ORIENTED_EDGE('',*,*,#3482,.F.);
#4719=ORIENTED_EDGE('',*,*,#3483,.T.);
#4720=ORIENTED_EDGE('',*,*,#3480,.T.);
#4721=ORIENTED_EDGE('',*,*,#3483,.F.);
#4722=ORIENTED_EDGE('',*,*,#3482,.T.);
#4723=ORIENTED_EDGE('',*,*,#3484,.F.);
#4724=ORIENTED_EDGE('',*,*,#3485,.F.);
#4725=ORIENTED_EDGE('',*,*,#3486,.T.);
#4726=ORIENTED_EDGE('',*,*,#3484,.T.);
#4727=ORIENTED_EDGE('',*,*,#3486,.F.);
#4728=ORIENTED_EDGE('',*,*,#3476,.T.);
#4729=ORIENTED_EDGE('',*,*,#3487,.T.);
#4730=ORIENTED_EDGE('',*,*,#3485,.T.);
#4731=ORIENTED_EDGE('',*,*,#3487,.F.);
#5264=CYLINDRICAL_SURFACE('',#6458,0.35);
#5265=CYLINDRICAL_SURFACE('',#6466,0.1954);
#5531=ADVANCED_FACE('',(#888),#589,.F.);
#5532=ADVANCED_FACE('',(#889),#590,.F.);
#5533=ADVANCED_FACE('',(#890),#591,.F.);
#5534=ADVANCED_FACE('',(#891),#592,.F.);
#5535=ADVANCED_FACE('',(#892),#593,.F.);
#5536=ADVANCED_FACE('',(#893),#594,.F.);
#5537=ADVANCED_FACE('',(#894),#595,.F.);
#5538=ADVANCED_FACE('',(#895),#596,.F.);
#5539=ADVANCED_FACE('',(#896),#597,.F.);
#5540=ADVANCED_FACE('',(#897),#598,.T.);
#5541=ADVANCED_FACE('',(#898),#203,.T.);
#5542=ADVANCED_FACE('',(#899),#5264,.T.);
#5543=ADVANCED_FACE('',(#900),#204,.T.);
#5544=ADVANCED_FACE('',(#901,#454),#599,.T.);
#5545=ADVANCED_FACE('',(#902),#205,.T.);
#5546=ADVANCED_FACE('',(#903),#5265,.T.);
#5657=CLOSED_SHELL('',(#5531,#5532,#5533,#5534,#5535,#5536,#5537,#5538));
#5658=CLOSED_SHELL('',(#5539,#5540,#5541,#5542,#5543,#5544,#5545,#5546));
#6443=AXIS2_PLACEMENT_3D('',#10101,#7897,#7898);
#6444=AXIS2_PLACEMENT_3D('',#10102,#7899,#7900);
#6445=AXIS2_PLACEMENT_3D('',#10111,#7905,#7906);
#6446=AXIS2_PLACEMENT_3D('',#10117,#7910,#7911);
#6447=AXIS2_PLACEMENT_3D('',#10123,#7915,#7916);
#6448=AXIS2_PLACEMENT_3D('',#10129,#7920,#7921);
#6449=AXIS2_PLACEMENT_3D('',#10135,#7925,#7926);
#6450=AXIS2_PLACEMENT_3D('',#10138,#7929,#7930);
#6451=AXIS2_PLACEMENT_3D('',#10139,#7931,#7932);
#6452=AXIS2_PLACEMENT_3D('',#10140,#7933,#7934);
#6453=AXIS2_PLACEMENT_3D('',#10142,#7935,#7936);
#6454=AXIS2_PLACEMENT_3D('',#10143,#7937,#7938);
#6455=AXIS2_PLACEMENT_3D('',#10145,#7939,#7940);
#6456=AXIS2_PLACEMENT_3D('',#10146,#7941,#7942);
#6457=AXIS2_PLACEMENT_3D('',#10148,#7943,#7944);
#6458=AXIS2_PLACEMENT_3D('',#10150,#7946,#7947);
#6459=AXIS2_PLACEMENT_3D('',#10152,#7948,#7949);
#6460=AXIS2_PLACEMENT_3D('',#10154,#7951,#7952);
#6461=AXIS2_PLACEMENT_3D('',#10156,#7953,#7954);
#6462=AXIS2_PLACEMENT_3D('',#10158,#7956,#7957);
#6463=AXIS2_PLACEMENT_3D('',#10160,#7958,#7959);
#6464=AXIS2_PLACEMENT_3D('',#10161,#7960,#7961);
#6465=AXIS2_PLACEMENT_3D('',#10163,#7962,#7963);
#6466=AXIS2_PLACEMENT_3D('',#10165,#7965,#7966);
#7897=DIRECTION('axis',(0.,0.,1.));
#7898=DIRECTION('refdir',(1.,0.,0.));
#7899=DIRECTION('center_axis',(0.866025403784439,0.,-0.5));
#7900=DIRECTION('ref_axis',(0.5,0.,0.866025403784439));
#7901=DIRECTION('',(-0.5,0.,-0.866025403784439));
#7902=DIRECTION('',(0.,-1.,0.));
#7903=DIRECTION('',(0.5,0.,0.866025403784439));
#7904=DIRECTION('',(0.,-1.,0.));
#7905=DIRECTION('center_axis',(1.60246890531964E-16,0.,-1.));
#7906=DIRECTION('ref_axis',(1.,0.,1.60246890531964E-16));
#7907=DIRECTION('',(-1.,0.,-1.60246890531964E-16));
#7908=DIRECTION('',(0.,-1.,0.));
#7909=DIRECTION('',(1.,0.,1.60246890531964E-16));
#7910=DIRECTION('center_axis',(-0.866025403784439,0.,-0.5));
#7911=DIRECTION('ref_axis',(0.5,0.,-0.866025403784439));
#7912=DIRECTION('',(-0.5,0.,0.866025403784439));
#7913=DIRECTION('',(0.,-1.,0.));
#7914=DIRECTION('',(0.5,0.,-0.866025403784439));
#7915=DIRECTION('center_axis',(-0.866025403784439,0.,0.5));
#7916=DIRECTION('ref_axis',(-0.5,0.,-0.866025403784439));
#7917=DIRECTION('',(0.5,0.,0.866025403784439));
#7918=DIRECTION('',(0.,-1.,0.));
#7919=DIRECTION('',(-0.5,0.,-0.866025403784439));
#7920=DIRECTION('center_axis',(-1.60246890531964E-16,0.,1.));
#7921=DIRECTION('ref_axis',(-1.,0.,-1.60246890531964E-16));
#7922=DIRECTION('',(1.,0.,1.60246890531964E-16));
#7923=DIRECTION('',(0.,-1.,0.));
#7924=DIRECTION('',(-1.,0.,-1.60246890531964E-16));
#7925=DIRECTION('center_axis',(0.866025403784439,0.,0.5));
#7926=DIRECTION('ref_axis',(-0.5,0.,0.866025403784439));
#7927=DIRECTION('',(0.5,0.,-0.866025403784439));
#7928=DIRECTION('',(-0.5,0.,0.866025403784439));
#7929=DIRECTION('center_axis',(0.,1.,0.));
#7930=DIRECTION('ref_axis',(1.,0.,0.));
#7931=DIRECTION('center_axis',(0.,-1.,0.));
#7932=DIRECTION('ref_axis',(0.,0.,-1.));
#7933=DIRECTION('center_axis',(0.,1.,0.));
#7934=DIRECTION('ref_axis',(1.,0.,0.));
#7935=DIRECTION('center_axis',(0.,1.,0.));
#7936=DIRECTION('ref_axis',(1.,0.,0.));
#7937=DIRECTION('center_axis',(0.,1.,0.));
#7938=DIRECTION('ref_axis',(0.,0.,1.));
#7939=DIRECTION('center_axis',(0.,-1.,0.));
#7940=DIRECTION('ref_axis',(1.,0.,0.));
#7941=DIRECTION('center_axis',(0.,-1.,0.));
#7942=DIRECTION('ref_axis',(1.,0.,0.));
#7943=DIRECTION('center_axis',(0.,-1.,0.));
#7944=DIRECTION('ref_axis',(1.,0.,0.));
#7945=DIRECTION('',(0.707106781186547,0.707106781186548,8.65956056235493E-17));
#7946=DIRECTION('center_axis',(0.,-1.,0.));
#7947=DIRECTION('ref_axis',(1.,0.,0.));
#7948=DIRECTION('center_axis',(0.,-1.,0.));
#7949=DIRECTION('ref_axis',(1.,0.,0.));
#7950=DIRECTION('',(0.,1.,0.));
#7951=DIRECTION('center_axis',(0.,1.,0.));
#7952=DIRECTION('ref_axis',(1.,0.,0.));
#7953=DIRECTION('center_axis',(0.,-1.,0.));
#7954=DIRECTION('ref_axis',(1.,0.,0.));
#7955=DIRECTION('',(-0.707106781186547,0.707106781186548,-8.65956056235493E-17));
#7956=DIRECTION('center_axis',(0.,-1.,0.));
#7957=DIRECTION('ref_axis',(0.,0.,-1.));
#7958=DIRECTION('center_axis',(0.,-1.,0.));
#7959=DIRECTION('ref_axis',(1.,0.,0.));
#7960=DIRECTION('center_axis',(0.,1.,0.));
#7961=DIRECTION('ref_axis',(1.,0.,0.));
#7962=DIRECTION('center_axis',(0.,1.,0.));
#7963=DIRECTION('ref_axis',(1.,0.,0.));
#7964=DIRECTION('',(-0.447213595499958,0.894427190999916,-5.47678698264203E-17));
#7965=DIRECTION('center_axis',(0.,-1.,0.));
#7966=DIRECTION('ref_axis',(1.,0.,0.));
#7967=DIRECTION('',(0.,1.,0.));
#10101=CARTESIAN_POINT('',(0.,0.,0.));
#10102=CARTESIAN_POINT('Origin',(0.0866025403784439,-0.4,-0.15));
#10103=CARTESIAN_POINT('',(0.173205080756888,-0.4,0.));
#10104=CARTESIAN_POINT('',(0.0866025403784439,-0.4,-0.15));
#10105=CARTESIAN_POINT('',(0.173205080756888,-0.4,0.));
#10106=CARTESIAN_POINT('',(0.0866025403784439,-0.64,-0.15));
#10107=CARTESIAN_POINT('',(0.0866025403784439,-0.4,-0.15));
#10108=CARTESIAN_POINT('',(0.173205080756888,-0.64,0.));
#10109=CARTESIAN_POINT('',(0.173205080756888,-0.64,0.));
#10110=CARTESIAN_POINT('',(0.173205080756888,-0.4,0.));
#10111=CARTESIAN_POINT('Origin',(-0.0866025403784438,-0.4,-0.15));
#10112=CARTESIAN_POINT('',(-0.0866025403784438,-0.4,-0.15));
#10113=CARTESIAN_POINT('',(0.0866025403784439,-0.4,-0.15));
#10114=CARTESIAN_POINT('',(-0.0866025403784438,-0.64,-0.15));
#10115=CARTESIAN_POINT('',(-0.0866025403784438,-0.4,-0.15));
#10116=CARTESIAN_POINT('',(0.0866025403784439,-0.64,-0.15));
#10117=CARTESIAN_POINT('Origin',(-0.173205080756888,-0.4,-2.77555756156289E-17));
#10118=CARTESIAN_POINT('',(-0.173205080756888,-0.4,-2.12115047744981E-17));
#10119=CARTESIAN_POINT('',(-0.0866025403784438,-0.4,-0.15));
#10120=CARTESIAN_POINT('',(-0.173205080756888,-0.64,-2.77555756156289E-17));
#10121=CARTESIAN_POINT('',(-0.173205080756888,-0.4,-2.12115047744981E-17));
#10122=CARTESIAN_POINT('',(-0.0866025403784438,-0.64,-0.15));
#10123=CARTESIAN_POINT('Origin',(-0.0866025403784439,-0.4,0.15));
#10124=CARTESIAN_POINT('',(-0.0866025403784439,-0.4,0.15));
#10125=CARTESIAN_POINT('',(-0.173205080756888,-0.4,-2.12115047744981E-17));
#10126=CARTESIAN_POINT('',(-0.0866025403784439,-0.64,0.15));
#10127=CARTESIAN_POINT('',(-0.0866025403784439,-0.4,0.15));
#10128=CARTESIAN_POINT('',(-0.173205080756888,-0.64,-2.12115047744981E-17));
#10129=CARTESIAN_POINT('Origin',(0.0866025403784439,-0.4,0.15));
#10130=CARTESIAN_POINT('',(0.0866025403784439,-0.4,0.15));
#10131=CARTESIAN_POINT('',(-0.0866025403784439,-0.4,0.15));
#10132=CARTESIAN_POINT('',(0.0866025403784439,-0.64,0.15));
#10133=CARTESIAN_POINT('',(0.0866025403784439,-0.4,0.15));
#10134=CARTESIAN_POINT('',(-0.0866025403784439,-0.64,0.15));
#10135=CARTESIAN_POINT('Origin',(0.173205080756888,-0.4,0.));
#10136=CARTESIAN_POINT('',(0.0866025403784439,-0.4,0.15));
#10137=CARTESIAN_POINT('',(0.0866025403784439,-0.64,0.15));
#10138=CARTESIAN_POINT('Origin',(0.,-0.4,-2.77555756156289E-17));
#10139=CARTESIAN_POINT('Origin',(0.,-0.64,-2.77555756156289E-17));
#10140=CARTESIAN_POINT('Origin',(0.,-1.,0.));
#10141=CARTESIAN_POINT('',(-0.1954,-1.,2.39295984553393E-17));
#10142=CARTESIAN_POINT('Origin',(0.,-1.,0.));
#10143=CARTESIAN_POINT('Origin',(0.3,0.4,0.));
#10144=CARTESIAN_POINT('',(-0.3,0.4,-3.67394039744206E-17));
#10145=CARTESIAN_POINT('Origin',(0.,0.4,0.));
#10146=CARTESIAN_POINT('Origin',(0.,0.375,0.));
#10147=CARTESIAN_POINT('',(-0.35,0.35,-4.28626379701573E-17));
#10148=CARTESIAN_POINT('Origin',(0.,0.35,0.));
#10149=CARTESIAN_POINT('',(-0.325,0.375,-3.9801020972289E-17));
#10150=CARTESIAN_POINT('Origin',(0.,0.19,0.));
#10151=CARTESIAN_POINT('',(-0.35,0.03,-4.28626379701574E-17));
#10152=CARTESIAN_POINT('Origin',(0.,0.03,0.));
#10153=CARTESIAN_POINT('',(-0.35,0.19,-4.28626379701574E-17));
#10154=CARTESIAN_POINT('Origin',(0.,0.0149999999999999,0.));
#10155=CARTESIAN_POINT('',(-0.32,-3.29597460435593E-17,-3.91886975727153E-17));
#10156=CARTESIAN_POINT('Origin',(0.,0.,0.));
#10157=CARTESIAN_POINT('',(-0.335,0.0149999999999999,-4.10256677714363E-17));
#10158=CARTESIAN_POINT('Origin',(0.22,0.,0.));
#10159=CARTESIAN_POINT('',(-0.22,-6.93889390390723E-18,-2.69422295812418E-17));
#10160=CARTESIAN_POINT('Origin',(0.,0.,0.));
#10161=CARTESIAN_POINT('Origin',(0.,-0.02,0.));
#10162=CARTESIAN_POINT('',(-0.1954,-0.0492,2.39295984553393E-17));
#10163=CARTESIAN_POINT('Origin',(0.,-0.0492,0.));
#10164=CARTESIAN_POINT('',(-0.21,-0.02,-2.57175827820944E-17));
#10165=CARTESIAN_POINT('Origin',(0.,-0.8,0.));
#10166=CARTESIAN_POINT('',(-0.1954,-0.8,-2.39295984553393E-17));
#10801=UNCERTAINTY_MEASURE_WITH_UNIT(LENGTH_MEASURE(0.001),#10838,
'DISTANCE_ACCURACY_VALUE',
'Maximum model space distance between geometric entities at asserted c
onnectivities');
#10807=UNCERTAINTY_MEASURE_WITH_UNIT(LENGTH_MEASURE(0.001),#10838,
'DISTANCE_ACCURACY_VALUE',
'Maximum model space distance between geometric entities at asserted c
onnectivities');
#10831=(
GEOMETRIC_REPRESENTATION_CONTEXT(3)
GLOBAL_UNCERTAINTY_ASSIGNED_CONTEXT((#10801))
GLOBAL_UNIT_ASSIGNED_CONTEXT((#10838,#10840,#10841))
REPRESENTATION_CONTEXT('','3D')
);
#10837=(
GEOMETRIC_REPRESENTATION_CONTEXT(3)
GLOBAL_UNCERTAINTY_ASSIGNED_CONTEXT((#10807))
GLOBAL_UNIT_ASSIGNED_CONTEXT((#10838,#10840,#10841))
REPRESENTATION_CONTEXT('','3D')
);
#10838=(
LENGTH_UNIT()
NAMED_UNIT(*)
SI_UNIT(.CENTI.,.METRE.)
);
#10840=(
NAMED_UNIT(*)
PLANE_ANGLE_UNIT()
SI_UNIT($,.RADIAN.)
);
#10841=(
NAMED_UNIT(*)
SI_UNIT($,.STERADIAN.)
SOLID_ANGLE_UNIT()
);
#10865=SHAPE_DEFINITION_REPRESENTATION(#10899,#10964);
#10899=PRODUCT_DEFINITION_SHAPE('',$,#10994);
#10964=SHAPE_REPRESENTATION('',(#6443),#10831);
#10970=PRODUCT_DEFINITION_CONTEXT('part definition',#11059,'design');
#10994=PRODUCT_DEFINITION('M4x10 Cap Screw','M4x10 Cap Screw',#11023,#10970);
#11023=PRODUCT_DEFINITION_FORMATION('',$,#11084);
#11059=APPLICATION_CONTEXT(
'Core Data for Automotive Mechanical Design Process');
#11060=PRODUCT_CONTEXT('part definition',#11059,'mechanical');
#11084=PRODUCT('M4x10 Cap Screw','M4x10 Cap Screw','M4x10 Cap Screw',(#11060));
#11167=COLOUR_RGB('Black',0.12,0.14,0.17);
#11168=FILL_AREA_STYLE_COLOUR('',#11167);
#11169=FILL_AREA_STYLE('',(#11168));
#11170=SURFACE_STYLE_FILL_AREA(#11169);
#11171=SURFACE_SIDE_STYLE('',(#11170));
#11172=SURFACE_STYLE_USAGE(.BOTH.,#11171);
#11173=PRESENTATION_STYLE_ASSIGNMENT((#11172));
ENDSEC;
END-ISO-10303-21;
